ISO-10303-21;
HEADER;
FILE_DESCRIPTION (('STEP AP214'),
    '1' );
FILE_NAME ('Adapter Flange Plate.step',
    '2026-10-07T17:53:07',
    ( '' ),
    ( '' ),
    'SwSTEP 2.0',
    'SolidWorks 2025',
    '' );
FILE_SCHEMA (( 'AUTOMOTIVE_DESIGN' ));
ENDSEC;

DATA;
#14=EDGE_CURVE ( 'NONE', #8213, #13437, #9334, .T. ) ;
#39=FACE_BOUND ( 'NONE', #10748, .T. ) ;
#52=DIRECTION ( 'NONE',  ( 0.000000000000000000, 0.000000000000000000, 1.000000000000000000 ) ) ;
#67=CARTESIAN_POINT ( 'NONE',  ( 6.940811704950004213, 32.97290950744599769, 10.00000000000000000 ) ) ;
#68=VERTEX_POINT ( 'NONE', #167 ) ;
#111=EDGE_CURVE ( 'NONE', #2836, #5819, #1718, .T. ) ;
#137=DIRECTION ( 'NONE',  ( -0.000000000000000000, -0.000000000000000000, -1.000000000000000000 ) ) ;
#156=FACE_OUTER_BOUND ( 'NONE', #2583, .T. ) ;
#158=AXIS2_PLACEMENT_3D ( 'NONE', #4444, #13785, #5467 ) ;
#167=CARTESIAN_POINT ( 'NONE',  ( -32.05918829504999934, 27.97290950744599769, 10.00000000000000000 ) ) ;
#170=AXIS2_PLACEMENT_3D ( 'NONE', #9398, #10575, #4153 ) ;
#186=ADVANCED_FACE ( 'NONE', ( #7633, #11914, #39, #5265, #12757, #7419 ), #11708, .T. ) ;
#201=ORIENTED_EDGE ( 'NONE', *, *, #8919, .T. ) ;
#222=ORIENTED_EDGE ( 'NONE', *, *, #6909, .F. ) ;
#246=EDGE_LOOP ( 'NONE', ( #8019, #3663 ) ) ;
#266=CIRCLE ( 'NONE', #12968, 3.000000000000002665 ) ;
#279=EDGE_CURVE ( 'NONE', #9088, #13769, #8829, .T. ) ;
#296=EDGE_CURVE ( 'NONE', #13765, #13437, #12321, .T. ) ;
#314=DIRECTION ( 'NONE',  ( -1.000000000000000000, 0.000000000000000000, 0.000000000000000000 ) ) ;
#337=ORIENTED_EDGE ( 'NONE', *, *, #13214, .F. ) ;
#346=VECTOR ( 'NONE', #9572, 1000.000000000000000 ) ;
#354=CYLINDRICAL_SURFACE ( 'NONE', #1490, 6.049999999999999822 ) ;
#361=AXIS2_PLACEMENT_3D ( 'NONE', #9633, #52, #5763 ) ;
#367=ORIENTED_EDGE ( 'NONE', *, *, #7268, .F. ) ;
#369=EDGE_CURVE ( 'NONE', #9649, #5856, #6141, .T. ) ;
#376=EDGE_LOOP ( 'NONE', ( #13002, #6845, #9254, #779 ) ) ;
#417=CIRCLE ( 'NONE', #4437, 1.499999999999999556 ) ;
#445=AXIS2_PLACEMENT_3D ( 'NONE', #10538, #7564, #4179 ) ;
#454=ORIENTED_EDGE ( 'NONE', *, *, #13612, .T. ) ;
#463=PRODUCT ( 'Adapter Flange Plate', 'Adapter Flange Plate', '', ( #9677 ) ) ;
#487=CIRCLE ( 'NONE', #12751, 2.999999999999998224 ) ;
#488=TOROIDAL_SURFACE ( 'NONE', #8290, 20.00000000000000000, 1.500000000000000000 ) ;
#489=EDGE_CURVE ( 'NONE', #2763, #3609, #10908, .T. ) ;
#496=DIRECTION ( 'NONE',  ( 1.000000000000000000, 0.000000000000000000, 0.000000000000000000 ) ) ;
#498=CYLINDRICAL_SURFACE ( 'NONE', #6914, 3.000000000000000000 ) ;
#510=VERTEX_POINT ( 'NONE', #1250 ) ;
#551=CARTESIAN_POINT ( 'NONE',  ( -36.55918829504999934, 10.97290950744599947, 11.50000000000000000 ) ) ;
#559=EDGE_CURVE ( 'NONE', #9088, #7612, #6024, .T. ) ;
#619=ORIENTED_EDGE ( 'NONE', *, *, #11776, .F. ) ;
#638=ORIENTED_EDGE ( 'NONE', *, *, #6718, .T. ) ;
#645=VECTOR ( 'NONE', #9718, 1000.000000000000000 ) ;
#661=AXIS2_PLACEMENT_3D ( 'NONE', #13156, #2499, #314 ) ;
#663=ADVANCED_FACE ( 'NONE', ( #3779 ), #498, .F. ) ;
#669=EDGE_CURVE ( 'NONE', #8809, #5925, #7950, .T. ) ;
#720=ORIENTED_EDGE ( 'NONE', *, *, #2109, .T. ) ;
#726=DIRECTION ( 'NONE',  ( 1.000000000000000000, 0.000000000000000000, 0.000000000000000000 ) ) ;
#729=CARTESIAN_POINT ( 'NONE',  ( -18.05918829504999934, 10.97290950744599947, 11.50000000000000000 ) ) ;
#733=ORIENTED_EDGE ( 'NONE', *, *, #8919, .F. ) ;
#734=EDGE_CURVE ( 'NONE', #8809, #7757, #3151, .T. ) ;
#740=LINE ( 'NONE', #11291, #13292 ) ;
#755=VERTEX_POINT ( 'NONE', #6196 ) ;
#778=ORIENTED_EDGE ( 'NONE', *, *, #4763, .F. ) ;
#779=ORIENTED_EDGE ( 'NONE', *, *, #1207, .F. ) ;
#796=FACE_OUTER_BOUND ( 'NONE', #2619, .T. ) ;
#799=ORIENTED_EDGE ( 'NONE', *, *, #2109, .F. ) ;
#831=AXIS2_PLACEMENT_3D ( 'NONE', #2439, #13238, #7776 ) ;
#854=AXIS2_PLACEMENT_3D ( 'NONE', #5360, #1035, #3352 ) ;
#864=AXIS2_PLACEMENT_3D ( 'NONE', #13755, #12657, #3296 ) ;
#892=EDGE_CURVE ( 'NONE', #1393, #10499, #12776, .T. ) ;
#896=VECTOR ( 'NONE', #7716, 1000.000000000000000 ) ;
#906=CIRCLE ( 'NONE', #8713, 3.000000000000002665 ) ;
#908=AXIS2_PLACEMENT_3D ( 'NONE', #3569, #4603, #5491 ) ;
#938=ORIENTED_EDGE ( 'NONE', *, *, #296, .F. ) ;
#1002=DIRECTION ( 'NONE',  ( 1.224646799147353207E-16, 1.000000000000000000, -0.000000000000000000 ) ) ;
#1034=EDGE_LOOP ( 'NONE', ( #12440, #4018 ) ) ;
#1035=DIRECTION ( 'NONE',  ( -0.000000000000000000, -0.000000000000000000, -1.000000000000000000 ) ) ;
#1036=ADVANCED_FACE ( 'NONE', ( #10126 ), #4674, .F. ) ;
#1038=EDGE_CURVE ( 'NONE', #10499, #510, #906, .T. ) ;
#1043=ORIENTED_EDGE ( 'NONE', *, *, #8109, .F. ) ;
#1060=EDGE_CURVE ( 'NONE', #5576, #1179, #12296, .T. ) ;
#1068=FACE_OUTER_BOUND ( 'NONE', #8752, .T. ) ;
#1113=DIRECTION ( 'NONE',  ( 1.000000000000000000, 0.000000000000000000, 0.000000000000000000 ) ) ;
#1114=CARTESIAN_POINT ( 'NONE',  ( -43.05918829505001355, -11.02709049255400053, 0.000000000000000000 ) ) ;
#1121=ORIENTED_EDGE ( 'NONE', *, *, #8680, .T. ) ;
#1122=ORIENTED_EDGE ( 'NONE', *, *, #12876, .F. ) ;
#1135=EDGE_LOOP ( 'NONE', ( #7058, #3626, #8748, #2169 ) ) ;
#1148=CARTESIAN_POINT ( 'NONE',  ( -1.059188295049996231, -6.027090492554000534, 0.000000000000000000 ) ) ;
#1179=VERTEX_POINT ( 'NONE', #3901 ) ;
#1207=EDGE_CURVE ( 'NONE', #755, #1411, #11435, .T. ) ;
#1210=EDGE_LOOP ( 'NONE', ( #7018, #3341, #4736, #1690 ) ) ;
#1214=DIRECTION ( 'NONE',  ( 1.000000000000000000, 0.000000000000000000, -0.000000000000000000 ) ) ;
#1224=SHAPE_REPRESENTATION_RELATIONSHIP ( 'NONE' , 'NONE' ,  #5062, #3759 ) ;
#1250=CARTESIAN_POINT ( 'NONE',  ( -40.05918829504999934, -14.02709049255400053, 0.000000000000000000 ) ) ;
#1280=ORIENTED_EDGE ( 'NONE', *, *, #369, .F. ) ;
#1324=DIRECTION ( 'NONE',  ( 0.000000000000000000, 0.000000000000000000, 1.000000000000000000 ) ) ;
#1346=LINE ( 'NONE', #8753, #7979 ) ;
#1364=CARTESIAN_POINT ( 'NONE',  ( -18.05918829504999934, 10.97290950744599947, 11.50000000000000000 ) ) ;
#1375=EDGE_CURVE ( 'NONE', #8213, #9649, #487, .T. ) ;
#1393=VERTEX_POINT ( 'NONE', #4923 ) ;
#1399=CARTESIAN_POINT ( 'NONE',  ( -1.059188295049996231, 27.97290950744599769, 0.000000000000000000 ) ) ;
#1411=VERTEX_POINT ( 'NONE', #3949 ) ;
#1417=ORIENTED_EDGE ( 'NONE', *, *, #9988, .F. ) ;
#1454=DIRECTION ( 'NONE',  ( 1.000000000000000000, 0.000000000000000000, 0.000000000000000000 ) ) ;
#1461=VECTOR ( 'NONE', #2767, 1000.000000000000000 ) ;
#1463=DIRECTION ( 'NONE',  ( 0.000000000000000000, 0.000000000000000000, 1.000000000000000000 ) ) ;
#1490=AXIS2_PLACEMENT_3D ( 'NONE', #6835, #5787, #10070 ) ;
#1500=EDGE_CURVE ( 'NONE', #6209, #7736, #4425, .T. ) ;
#1505=TOROIDAL_SURFACE ( 'NONE', #9776, 16.99999999999999645, 1.500000000000000000 ) ;
#1506=ORIENTED_EDGE ( 'NONE', *, *, #489, .T. ) ;
#1518=DIRECTION ( 'NONE',  ( -0.000000000000000000, -0.000000000000000000, -1.000000000000000000 ) ) ;
#1520=DIRECTION ( 'NONE',  ( 0.000000000000000000, 0.000000000000000000, 1.000000000000000000 ) ) ;
#1547=AXIS2_PLACEMENT_3D ( 'NONE', #5114, #6150, #10357 ) ;
#1556=DIRECTION ( 'NONE',  ( -0.000000000000000000, -0.000000000000000000, -1.000000000000000000 ) ) ;
#1557=ORIENTED_EDGE ( 'NONE', *, *, #892, .T. ) ;
#1561=VECTOR ( 'NONE', #10811, 1000.000000000000000 ) ;
#1577=AXIS2_PLACEMENT_3D ( 'NONE', #2529, #11157, #11297 ) ;
#1586=VECTOR ( 'NONE', #9342, 1000.000000000000000 ) ;
#1587=VERTEX_POINT ( 'NONE', #8893 ) ;
#1607=FACE_OUTER_BOUND ( 'NONE', #10170, .T. ) ;
#1611=EDGE_CURVE ( 'NONE', #8462, #755, #266, .T. ) ;
#1622=CARTESIAN_POINT ( 'NONE',  ( 6.940811704950004213, 32.97290950744599769, 0.000000000000000000 ) ) ;
#1631=CARTESIAN_POINT ( 'NONE',  ( -18.05918829504999934, 10.97290950744599947, 10.00000000000000000 ) ) ;
#1645=AXIS2_PLACEMENT_3D ( 'NONE', #5776, #3696, #1454 ) ;
#1670=EDGE_LOOP ( 'NONE', ( #10777, #2517, #12810, #4417 ) ) ;
#1690=ORIENTED_EDGE ( 'NONE', *, *, #8139, .T. ) ;
#1716=CARTESIAN_POINT ( 'NONE',  ( -18.05918829504999934, 10.97290950744599947, 12.50000000000000000 ) ) ;
#1718=CIRCLE ( 'NONE', #158, 3.000000000000002665 ) ;
#1731=AXIS2_PLACEMENT_3D ( 'NONE', #5256, #12746, #13270 ) ;
#1772=DIRECTION ( 'NONE',  ( -1.000000000000000000, 0.000000000000000000, 0.000000000000000000 ) ) ;
#1846=AXIS2_PLACEMENT_3D ( 'NONE', #6539, #2228, #13666 ) ;
#1889=ORIENTED_EDGE ( 'NONE', *, *, #734, .T. ) ;
#1899=EDGE_CURVE ( 'NONE', #1411, #2899, #10959, .T. ) ;
#1904=DIRECTION ( 'NONE',  ( 0.000000000000000000, 0.000000000000000000, 1.000000000000000000 ) ) ;
#1930=AXIS2_PLACEMENT_3D ( 'NONE', #9743, #9681, #3265 ) ;
#1934=VERTEX_POINT ( 'NONE', #7327 ) ;
#2002=VERTEX_POINT ( 'NONE', #2739 ) ;
#2006=AXIS2_PLACEMENT_3D ( 'NONE', #3693, #137, #10128 ) ;
#2008=DIRECTION ( 'NONE',  ( 0.000000000000000000, 0.000000000000000000, 1.000000000000000000 ) ) ;
#2010=CARTESIAN_POINT ( 'NONE',  ( -1.059188295049996231, -6.027090492554000534, 0.000000000000000000 ) ) ;
#2032=CARTESIAN_POINT ( 'NONE',  ( -1.059188295049996231, 27.97290950744599769, 0.000000000000000000 ) ) ;
#2049=AXIS2_PLACEMENT_3D ( 'NONE', #4747, #1518, #5774 ) ;
#2059=ORIENTED_EDGE ( 'NONE', *, *, #3701, .T. ) ;
#2109=EDGE_CURVE ( 'NONE', #10331, #1179, #3825, .T. ) ;
#2138=EDGE_CURVE ( 'NONE', #12260, #2002, #4117, .T. ) ;
#2142=CYLINDRICAL_SURFACE ( 'NONE', #11765, 3.000000000000002665 ) ;
#2161=FACE_BOUND ( 'NONE', #12086, .T. ) ;
#2169=ORIENTED_EDGE ( 'NONE', *, *, #8109, .T. ) ;
#2190=DIRECTION ( 'NONE',  ( 0.000000000000000000, 0.000000000000000000, 1.000000000000000000 ) ) ;
#2195=CIRCLE ( 'NONE', #1731, 16.99999999999999645 ) ;
#2203=ORIENTED_EDGE ( 'NONE', *, *, #9709, .F. ) ;
#2222=DIRECTION ( 'NONE',  ( 0.000000000000000000, 0.000000000000000000, 1.000000000000000000 ) ) ;
#2228=DIRECTION ( 'NONE',  ( 0.000000000000000000, 0.000000000000000000, 1.000000000000000000 ) ) ;
#2249=CARTESIAN_POINT ( 'NONE',  ( 1.940811704950003991, 27.97290950744599769, 0.000000000000000000 ) ) ;
#2253=UNCERTAINTY_MEASURE_WITH_UNIT (LENGTH_MEASURE( 1.000000000000000082E-05 ), #2308, 'distance_accuracy_value', 'NONE');
#2269=CIRCLE ( 'NONE', #12058, 3.000000000000000000 ) ;
#2270=VECTOR ( 'NONE', #2974, 1000.000000000000000 ) ;
#2281=DIRECTION ( 'NONE',  ( -0.000000000000000000, -0.000000000000000000, 1.000000000000000000 ) ) ;
#2285=DIRECTION ( 'NONE',  ( -0.000000000000000000, -0.000000000000000000, -1.000000000000000000 ) ) ;
#2298=CARTESIAN_POINT ( 'NONE',  ( -38.05918829505000645, -6.027090492554000534, 0.000000000000000000 ) ) ;
#2307=CARTESIAN_POINT ( 'NONE',  ( -40.05918829504999934, -14.02709049255400053, 0.000000000000000000 ) ) ;
#2308=( LENGTH_UNIT ( ) NAMED_UNIT ( * ) SI_UNIT ( .MILLI., .METRE. ) );
#2312=EDGE_LOOP ( 'NONE', ( #12395, #12524, #11737, #10650 ) ) ;
#2335=ORIENTED_EDGE ( 'NONE', *, *, #6802, .T. ) ;
#2358=DIRECTION ( 'NONE',  ( -0.000000000000000000, -0.000000000000000000, 1.000000000000000000 ) ) ;
#2386=ORIENTED_EDGE ( 'NONE', *, *, #1899, .F. ) ;
#2387=CARTESIAN_POINT ( 'NONE',  ( -43.05918829505002066, 32.97290950744599769, 10.00000000000000000 ) ) ;
#2399=CIRCLE ( 'NONE', #7707, 3.000000000000002665 ) ;
#2439=CARTESIAN_POINT ( 'NONE',  ( -1.059188295049996231, -6.027090492554000534, 0.000000000000000000 ) ) ;
#2461=LINE ( 'NONE', #10891, #12983 ) ;
#2481=ORIENTED_EDGE ( 'NONE', *, *, #734, .F. ) ;
#2494=VERTEX_POINT ( 'NONE', #2719 ) ;
#2499=DIRECTION ( 'NONE',  ( -0.000000000000000000, -0.000000000000000000, -1.000000000000000000 ) ) ;
#2504=DIRECTION ( 'NONE',  ( 0.000000000000000000, 0.000000000000000000, 1.000000000000000000 ) ) ;
#2513=DIRECTION ( 'NONE',  ( 0.000000000000000000, 0.000000000000000000, 1.000000000000000000 ) ) ;
#2517=ORIENTED_EDGE ( 'NONE', *, *, #4829, .F. ) ;
#2529=CARTESIAN_POINT ( 'NONE',  ( -40.05918829504999934, -14.02709049255400053, 10.00000000000000000 ) ) ;
#2531=ORIENTED_EDGE ( 'NONE', *, *, #9709, .T. ) ;
#2548=EDGE_CURVE ( 'NONE', #2899, #1411, #8501, .T. ) ;
#2551=CARTESIAN_POINT ( 'NONE',  ( -43.05918829505002066, 32.97290950744599769, 10.00000000000000000 ) ) ;
#2556=EDGE_CURVE ( 'NONE', #7736, #5576, #4070, .T. ) ;
#2559=AXIS2_PLACEMENT_3D ( 'NONE', #11239, #1520, #10131 ) ;
#2574=SURFACE_STYLE_FILL_AREA ( #13299 ) ;
#2583=EDGE_LOOP ( 'NONE', ( #3306, #1122, #12219, #10903 ) ) ;
#2589=CARTESIAN_POINT ( 'NONE',  ( 0.4408117049500004381, 10.97290950744600124, 14.00000000000000000 ) ) ;
#2604=ORIENTED_EDGE ( 'NONE', *, *, #5041, .T. ) ;
#2608=CIRCLE ( 'NONE', #13502, 3.000000000000000000 ) ;
#2615=AXIS2_PLACEMENT_3D ( 'NONE', #13023, #2504, #7696 ) ;
#2619=EDGE_LOOP ( 'NONE', ( #5617, #11059, #4892, #12617 ) ) ;
#2629=AXIS2_PLACEMENT_3D ( 'NONE', #7810, #1463, #7037 ) ;
#2634=FACE_OUTER_BOUND ( 'NONE', #376, .T. ) ;
#2655=ADVANCED_FACE ( 'NONE', ( #796 ), #488, .F. ) ;
#2669=CIRCLE ( 'NONE', #4663, 2.999999999999999112 ) ;
#2672=VECTOR ( 'NONE', #3884, 1000.000000000000000 ) ;
#2698=PLANE ( 'NONE',  #8711 ) ;
#2715=DIRECTION ( 'NONE',  ( 0.000000000000000000, 0.000000000000000000, 1.000000000000000000 ) ) ;
#2719=CARTESIAN_POINT ( 'NONE',  ( -1.059188295050000894, 10.97290950744599947, 14.00000000000000000 ) ) ;
#2739=CARTESIAN_POINT ( 'NONE',  ( 1.940811704950003991, 27.97290950744599769, 10.00000000000000000 ) ) ;
#2763=VERTEX_POINT ( 'NONE', #7467 ) ;
#2767=DIRECTION ( 'NONE',  ( -1.182766006347823109E-16, 1.000000000000000000, -0.000000000000000000 ) ) ;
#2836=VERTEX_POINT ( 'NONE', #11699 ) ;
#2853=DIRECTION ( 'NONE',  ( 1.000000000000000000, 0.000000000000000000, 0.000000000000000000 ) ) ;
#2899=VERTEX_POINT ( 'NONE', #5811 ) ;
#2918=AXIS2_PLACEMENT_3D ( 'NONE', #13033, #10114, #9048 ) ;
#2948=EDGE_CURVE ( 'NONE', #1179, #10331, #8244, .T. ) ;
#2958=DIRECTION ( 'NONE',  ( 1.000000000000000000, 0.000000000000000000, 0.000000000000000000 ) ) ;
#2974=DIRECTION ( 'NONE',  ( -0.000000000000000000, -0.000000000000000000, -1.000000000000000000 ) ) ;
#2977=ORIENTED_EDGE ( 'NONE', *, *, #8408, .F. ) ;
#2997=DIRECTION ( 'NONE',  ( 0.000000000000000000, 0.000000000000000000, 1.000000000000000000 ) ) ;
#3002=EDGE_CURVE ( 'NONE', #1587, #6209, #6229, .T. ) ;
#3012=DIRECTION ( 'NONE',  ( -1.000000000000000000, 0.000000000000000000, 0.000000000000000000 ) ) ;
#3030=CYLINDRICAL_SURFACE ( 'NONE', #9554, 2.999999999999999112 ) ;
#3049=ORIENTED_EDGE ( 'NONE', *, *, #1038, .F. ) ;
#3051=EDGE_LOOP ( 'NONE', ( #9574, #10179, #6442, #7215 ) ) ;
#3079=CARTESIAN_POINT ( 'NONE',  ( 1.940811704950003991, -6.027090492554000534, 10.00000000000000000 ) ) ;
#3113=ORIENTED_EDGE ( 'NONE', *, *, #8680, .F. ) ;
#3136=ORIENTED_EDGE ( 'NONE', *, *, #6291, .F. ) ;
#3151=CIRCLE ( 'NONE', #4920, 3.000000000000002665 ) ;
#3181=DIRECTION ( 'NONE',  ( -1.000000000000000000, -1.182766006347823109E-16, 0.000000000000000000 ) ) ;
#3200=DIRECTION ( 'NONE',  ( 0.000000000000000000, 0.000000000000000000, 1.000000000000000000 ) ) ;
#3220=ORIENTED_EDGE ( 'NONE', *, *, #10227, .T. ) ;
#3265=DIRECTION ( 'NONE',  ( 1.000000000000000000, 0.000000000000000000, 0.000000000000000000 ) ) ;
#3296=DIRECTION ( 'NONE',  ( 1.000000000000000000, 0.000000000000000000, 0.000000000000000000 ) ) ;
#3306=ORIENTED_EDGE ( 'NONE', *, *, #6909, .T. ) ;
#3314=AXIS2_PLACEMENT_3D ( 'NONE', #5179, #3181, #4140 ) ;
#3315=CYLINDRICAL_SURFACE ( 'NONE', #11993, 3.000000000000000000 ) ;
#3341=ORIENTED_EDGE ( 'NONE', *, *, #5516, .F. ) ;
#3352=DIRECTION ( 'NONE',  ( -1.000000000000000000, 0.000000000000000000, 0.000000000000000000 ) ) ;
#3366=CARTESIAN_POINT ( 'NONE',  ( -1.059188295049996231, -6.027090492554000534, 0.000000000000000000 ) ) ;
#3413=FACE_BOUND ( 'NONE', #10987, .T. ) ;
#3447=ORIENTED_EDGE ( 'NONE', *, *, #1060, .T. ) ;
#3452=EDGE_LOOP ( 'NONE', ( #1417, #2203, #3447, #799 ) ) ;
#3457=ORIENTED_EDGE ( 'NONE', *, *, #13134, .T. ) ;
#3470=( NAMED_UNIT ( * ) SI_UNIT ( $, .STERADIAN. ) SOLID_ANGLE_UNIT ( ) );
#3490=LINE ( 'NONE', #5771, #6058 ) ;
#3498=CIRCLE ( 'NONE', #5040, 16.99999999999999645 ) ;
#3510=LINE ( 'NONE', #2551, #7346 ) ;
#3527=DIRECTION ( 'NONE',  ( 1.000000000000000000, 0.000000000000000000, 0.000000000000000000 ) ) ;
#3540=FILL_AREA_STYLE_COLOUR ( '', #3974 ) ;
#3545=CARTESIAN_POINT ( 'NONE',  ( -18.05918829504999934, 10.97290950744599947, 12.50000000000000000 ) ) ;
#3552=CIRCLE ( 'NONE', #13571, 6.049999999999999822 ) ;
#3557=CARTESIAN_POINT ( 'NONE',  ( -12.00918829504999863, 10.97290950744599947, 14.00000000000000000 ) ) ;
#3558=ORIENTED_EDGE ( 'NONE', *, *, #5948, .T. ) ;
#3569=CARTESIAN_POINT ( 'NONE',  ( -35.05918829505000645, -6.027090492554000534, 10.00000000000000000 ) ) ;
#3597=AXIS2_PLACEMENT_3D ( 'NONE', #5042, #10358, #10162 ) ;
#3609=VERTEX_POINT ( 'NONE', #3557 ) ;
#3626=ORIENTED_EDGE ( 'NONE', *, *, #5948, .F. ) ;
#3629=DIRECTION ( 'NONE',  ( -0.000000000000000000, -0.000000000000000000, -1.000000000000000000 ) ) ;
#3639=ADVANCED_FACE ( 'NONE', ( #5765 ), #12068, .F. ) ;
#3645=CARTESIAN_POINT ( 'NONE',  ( -32.05918829504999934, 27.97290950744599769, 0.000000000000000000 ) ) ;
#3663=ORIENTED_EDGE ( 'NONE', *, *, #6718, .F. ) ;
#3671=DIRECTION ( 'NONE',  ( 1.000000000000000000, 0.000000000000000000, 0.000000000000000000 ) ) ;
#3693=CARTESIAN_POINT ( 'NONE',  ( 3.940811704950003325, 32.97290950744599769, 10.00000000000000000 ) ) ;
#3696=DIRECTION ( 'NONE',  ( 0.000000000000000000, 0.000000000000000000, 1.000000000000000000 ) ) ;
#3701=EDGE_CURVE ( 'NONE', #1587, #5576, #6610, .T. ) ;
#3705=DIRECTION ( 'NONE',  ( -0.000000000000000000, -0.000000000000000000, 1.000000000000000000 ) ) ;
#3738=SURFACE_SIDE_STYLE ('',( #2574 ) ) ;
#3759=ADVANCED_BREP_SHAPE_REPRESENTATION ( '', ( #9762, #6434 ), #4214 ) ;
#3779=FACE_OUTER_BOUND ( 'NONE', #12319, .T. ) ;
#3781=DIRECTION ( 'NONE',  ( 0.000000000000000000, 0.000000000000000000, -1.000000000000000000 ) ) ;
#3782=APPLICATION_CONTEXT ( 'automotive_design' ) ;
#3824=EDGE_LOOP ( 'NONE', ( #7924, #7401, #454, #337 ) ) ;
#3825=CIRCLE ( 'NONE', #2049, 20.00000000000000000 ) ;
#3826=EDGE_CURVE ( 'NONE', #9617, #13769, #2269, .T. ) ;
#3884=DIRECTION ( 'NONE',  ( -1.000000000000000000, -0.000000000000000000, -0.000000000000000000 ) ) ;
#3901=CARTESIAN_POINT ( 'NONE',  ( 1.940811704950001770, 10.97290950744599947, 10.00000000000000000 ) ) ;
#3926=ORIENTED_EDGE ( 'NONE', *, *, #9962, .T. ) ;
#3949=CARTESIAN_POINT ( 'NONE',  ( -32.05918829504999934, -6.027090492554000534, 10.00000000000000000 ) ) ;
#3951=CARTESIAN_POINT ( 'NONE',  ( 3.940811704950009542, -14.02709049255400053, 0.000000000000000000 ) ) ;
#3974=COLOUR_RGB ( '', 0.09019608, 0.27058824, 0.51372549) ;
#3993=AXIS2_PLACEMENT_3D ( 'NONE', #12790, #2190, #1113 ) ;
#4001=ORIENTED_EDGE ( 'NONE', *, *, #12876, .T. ) ;
#4017=VERTEX_POINT ( 'NONE', #13663 ) ;
#4018=ORIENTED_EDGE ( 'NONE', *, *, #8442, .T. ) ;
#4032=AXIS2_PLACEMENT_3D ( 'NONE', #13778, #3200, #7412 ) ;
#4035=CARTESIAN_POINT ( 'NONE',  ( 6.940811704950001548, 32.97290950744599769, 10.00000000000000000 ) ) ;
#4057=ORIENTED_EDGE ( 'NONE', *, *, #892, .F. ) ;
#4070=CIRCLE ( 'NONE', #5594, 18.50000000000000000 ) ;
#4117=LINE ( 'NONE', #5273, #1586 ) ;
#4125=ORIENTED_EDGE ( 'NONE', *, *, #669, .T. ) ;
#4140=DIRECTION ( 'NONE',  ( 1.182766006347823109E-16, -1.000000000000000000, 0.000000000000000000 ) ) ;
#4153=DIRECTION ( 'NONE',  ( 1.000000000000000000, 0.000000000000000000, 0.000000000000000000 ) ) ;
#4158=DIRECTION ( 'NONE',  ( -0.000000000000000000, -0.000000000000000000, 1.000000000000000000 ) ) ;
#4166=ORIENTED_EDGE ( 'NONE', *, *, #10315, .F. ) ;
#4167=ADVANCED_FACE ( 'NONE', ( #8043, #12323 ), #2698, .T. ) ;
#4179=DIRECTION ( 'NONE',  ( 1.000000000000000000, 0.000000000000000000, -0.000000000000000000 ) ) ;
#4214=( GEOMETRIC_REPRESENTATION_CONTEXT ( 3 ) GLOBAL_UNCERTAINTY_ASSIGNED_CONTEXT ( ( #2253 ) ) GLOBAL_UNIT_ASSIGNED_CONTEXT ( ( #2308, #4454, #5276 ) ) REPRESENTATION_CONTEXT ( 'NONE', 'WORKASPACE' ) );
#4220=ORIENTED_EDGE ( 'NONE', *, *, #5959, .T. ) ;
#4248=EDGE_CURVE ( 'NONE', #2002, #7472, #10502, .T. ) ;
#4298=CARTESIAN_POINT ( 'NONE',  ( 3.940811704950010430, -11.02709049255400053, 10.00000000000000000 ) ) ;
#4299=DIRECTION ( 'NONE',  ( -1.000000000000000000, 0.000000000000000000, 0.000000000000000000 ) ) ;
#4319=DIRECTION ( 'NONE',  ( 0.000000000000000000, 0.000000000000000000, -1.000000000000000000 ) ) ;
#4321=AXIS2_PLACEMENT_3D ( 'NONE', #13431, #11337, #1772 ) ;
#4330=ORIENTED_EDGE ( 'NONE', *, *, #10739, .T. ) ;
#4367=CARTESIAN_POINT ( 'NONE',  ( -40.05918829505000645, 35.97290950744599058, 10.00000000000000000 ) ) ;
#4386=VERTEX_POINT ( 'NONE', #12724 ) ;
#4416=EDGE_LOOP ( 'NONE', ( #8535, #11635 ) ) ;
#4417=ORIENTED_EDGE ( 'NONE', *, *, #369, .T. ) ;
#4425=LINE ( 'NONE', #9734, #8728 ) ;
#4437=AXIS2_PLACEMENT_3D ( 'NONE', #12215, #6899, #7800 ) ;
#4444=CARTESIAN_POINT ( 'NONE',  ( -40.05918829504999934, -11.02709049255400053, 10.00000000000000000 ) ) ;
#4454=( NAMED_UNIT ( * ) PLANE_ANGLE_UNIT ( ) SI_UNIT ( $, .RADIAN. ) );
#4478=DIRECTION ( 'NONE',  ( -0.000000000000000000, -0.000000000000000000, 1.000000000000000000 ) ) ;
#4505=DIRECTION ( 'NONE',  ( -0.000000000000000000, -0.000000000000000000, -1.000000000000000000 ) ) ;
#4508=AXIS2_PLACEMENT_3D ( 'NONE', #6322, #12606, #8201 ) ;
#4532=CARTESIAN_POINT ( 'NONE',  ( 3.940811704950009542, -14.02709049255400053, 10.00000000000000000 ) ) ;
#4560=ORIENTED_EDGE ( 'NONE', *, *, #7709, .T. ) ;
#4572=CYLINDRICAL_SURFACE ( 'NONE', #661, 18.50000000000000000 ) ;
#4603=DIRECTION ( 'NONE',  ( 0.000000000000000000, 0.000000000000000000, 1.000000000000000000 ) ) ;
#4663=AXIS2_PLACEMENT_3D ( 'NONE', #4298, #7459, #10784 ) ;
#4674=PLANE ( 'NONE',  #1577 ) ;
#4700=VECTOR ( 'NONE', #3671, 1000.000000000000000 ) ;
#4714=DIRECTION ( 'NONE',  ( 0.000000000000000000, 0.000000000000000000, 1.000000000000000000 ) ) ;
#4736=ORIENTED_EDGE ( 'NONE', *, *, #11455, .F. ) ;
#4740=DIRECTION ( 'NONE',  ( -1.577021341797097560E-16, 1.000000000000000000, 0.000000000000000000 ) ) ;
#4747=CARTESIAN_POINT ( 'NONE',  ( -18.05918829504999934, 10.97290950744599947, 10.00000000000000000 ) ) ;
#4756=CARTESIAN_POINT ( 'NONE',  ( 1.940811704950003991, -6.027090492554000534, 0.000000000000000000 ) ) ;
#4763=EDGE_CURVE ( 'NONE', #8462, #2899, #2461, .T. ) ;
#4773=CIRCLE ( 'NONE', #1645, 3.000000000000000000 ) ;
#4802=CARTESIAN_POINT ( 'NONE',  ( 1.940811704950001770, 10.97290950744599947, 11.50000000000000000 ) ) ;
#4828=VECTOR ( 'NONE', #7965, 1000.000000000000000 ) ;
#4829=EDGE_CURVE ( 'NONE', #4386, #6747, #3490, .T. ) ;
#4846=ORIENTED_EDGE ( 'NONE', *, *, #2948, .T. ) ;
#4851=ORIENTED_EDGE ( 'NONE', *, *, #1899, .T. ) ;
#4892=ORIENTED_EDGE ( 'NONE', *, *, #2948, .F. ) ;
#4895=DIRECTION ( 'NONE',  ( -0.000000000000000000, -0.000000000000000000, 1.000000000000000000 ) ) ;
#4902=AXIS2_PLACEMENT_3D ( 'NONE', #1631, #9947, #12043 ) ;
#4920=AXIS2_PLACEMENT_3D ( 'NONE', #12641, #5162, #11666 ) ;
#4923=CARTESIAN_POINT ( 'NONE',  ( -43.05918829505002066, 32.97290950744599769, 0.000000000000000000 ) ) ;
#4943=DIRECTION ( 'NONE',  ( -0.000000000000000000, -0.000000000000000000, 1.000000000000000000 ) ) ;
#4962=CARTESIAN_POINT ( 'NONE',  ( 3.940811704950010430, -11.02709049255400053, 10.00000000000000000 ) ) ;
#4999=DIRECTION ( 'NONE',  ( -0.000000000000000000, -0.000000000000000000, 1.000000000000000000 ) ) ;
#5040=AXIS2_PLACEMENT_3D ( 'NONE', #12683, #7474, #9474 ) ;
#5041=EDGE_CURVE ( 'NONE', #13769, #9617, #10103, .T. ) ;
#5042=CARTESIAN_POINT ( 'NONE',  ( -40.05918829505000645, 32.97290950744599769, 0.000000000000000000 ) ) ;
#5062=SHAPE_REPRESENTATION ( 'Adapter Flange Plate', ( #6434 ), #4214 ) ;
#5093=CIRCLE ( 'NONE', #5963, 3.000000000000002665 ) ;
#5110=PLANE ( 'NONE',  #3314 ) ;
#5114=CARTESIAN_POINT ( 'NONE',  ( -18.05918829504999934, 10.97290950744599947, 12.50000000000000000 ) ) ;
#5133=VECTOR ( 'NONE', #10139, 1000.000000000000000 ) ;
#5161=CARTESIAN_POINT ( 'NONE',  ( -35.05918829505000645, -6.027090492554000534, 0.000000000000000000 ) ) ;
#5162=DIRECTION ( 'NONE',  ( 0.000000000000000000, 0.000000000000000000, 1.000000000000000000 ) ) ;
#5179=CARTESIAN_POINT ( 'NONE',  ( 6.940811704950004213, 32.97290950744599769, 10.00000000000000000 ) ) ;
#5197=DIRECTION ( 'NONE',  ( 1.000000000000000000, 0.000000000000000000, 0.000000000000000000 ) ) ;
#5206=ORIENTED_EDGE ( 'NONE', *, *, #9015, .T. ) ;
#5250=DIRECTION ( 'NONE',  ( 0.000000000000000000, 0.000000000000000000, 1.000000000000000000 ) ) ;
#5252=CIRCLE ( 'NONE', #11068, 18.50000000000000000 ) ;
#5256=CARTESIAN_POINT ( 'NONE',  ( -18.05918829504999934, 10.97290950744599947, 14.00000000000000000 ) ) ;
#5265=FACE_BOUND ( 'NONE', #11806, .T. ) ;
#5273=CARTESIAN_POINT ( 'NONE',  ( 1.940811704950003991, 27.97290950744599769, 0.000000000000000000 ) ) ;
#5276=( NAMED_UNIT ( * ) SI_UNIT ( $, .STERADIAN. ) SOLID_ANGLE_UNIT ( ) );
#5294=AXIS2_PLACEMENT_3D ( 'NONE', #1364, #2715, #10106 ) ;
#5296=LINE ( 'NONE', #67, #346 ) ;
#5303=CIRCLE ( 'NONE', #170, 6.049999999999999822 ) ;
#5318=TOROIDAL_SURFACE ( 'NONE', #3993, 16.99999999999999645, 1.500000000000000000 ) ;
#5335=CARTESIAN_POINT ( 'NONE',  ( -40.05918829504999934, -11.02709049255400053, 10.00000000000000000 ) ) ;
#5342=CARTESIAN_POINT ( 'NONE',  ( -18.05918829504999934, 10.97290950744599947, 14.00000000000000000 ) ) ;
#5360=CARTESIAN_POINT ( 'NONE',  ( -40.05918829504999934, -11.02709049255400053, 10.00000000000000000 ) ) ;
#5436=EDGE_LOOP ( 'NONE', ( #3049, #4057, #222, #5936, #9695, #938, #11323, #3136 ) ) ;
#5443=ORIENTED_EDGE ( 'NONE', *, *, #4248, .T. ) ;
#5452=DIRECTION ( 'NONE',  ( -1.000000000000000000, 0.000000000000000000, 0.000000000000000000 ) ) ;
#5464=ORIENTED_EDGE ( 'NONE', *, *, #8408, .T. ) ;
#5467=DIRECTION ( 'NONE',  ( 1.000000000000000000, 0.000000000000000000, 0.000000000000000000 ) ) ;
#5488=ORIENTED_EDGE ( 'NONE', *, *, #111, .F. ) ;
#5491=DIRECTION ( 'NONE',  ( 1.000000000000000000, 0.000000000000000000, 0.000000000000000000 ) ) ;
#5504=VECTOR ( 'NONE', #5681, 1000.000000000000000 ) ;
#5515=EDGE_LOOP ( 'NONE', ( #7881, #5464, #7910, #11430 ) ) ;
#5516=EDGE_CURVE ( 'NONE', #11194, #13765, #6583, .T. ) ;
#5526=AXIS2_PLACEMENT_3D ( 'NONE', #2032, #9487, #13526 ) ;
#5576=VERTEX_POINT ( 'NONE', #13289 ) ;
#5594=AXIS2_PLACEMENT_3D ( 'NONE', #729, #2997, #2853 ) ;
#5617=ORIENTED_EDGE ( 'NONE', *, *, #2556, .F. ) ;
#5626=ADVANCED_FACE ( 'NONE', ( #12388 ), #11271, .T. ) ;
#5681=DIRECTION ( 'NONE',  ( -0.000000000000000000, -0.000000000000000000, -1.000000000000000000 ) ) ;
#5715=CYLINDRICAL_SURFACE ( 'NONE', #8183, 3.000000000000000000 ) ;
#5763=DIRECTION ( 'NONE',  ( 1.000000000000000000, 0.000000000000000000, 0.000000000000000000 ) ) ;
#5765=FACE_OUTER_BOUND ( 'NONE', #9954, .T. ) ;
#5771=CARTESIAN_POINT ( 'NONE',  ( -40.05918829505000645, 35.97290950744599769, 10.00000000000000000 ) ) ;
#5774=DIRECTION ( 'NONE',  ( 1.000000000000000000, 0.000000000000000000, 0.000000000000000000 ) ) ;
#5776=CARTESIAN_POINT ( 'NONE',  ( -1.059188295049996231, 27.97290950744599769, 0.000000000000000000 ) ) ;
#5787=DIRECTION ( 'NONE',  ( -0.000000000000000000, -0.000000000000000000, 1.000000000000000000 ) ) ;
#5802=VECTOR ( 'NONE', #13562, 1000.000000000000000 ) ;
#5811=CARTESIAN_POINT ( 'NONE',  ( -38.05918829505000645, -6.027090492554000534, 10.00000000000000000 ) ) ;
#5819=VERTEX_POINT ( 'NONE', #9383 ) ;
#5827=LINE ( 'NONE', #10112, #5504 ) ;
#5829=CYLINDRICAL_SURFACE ( 'NONE', #2918, 3.000000000000002665 ) ;
#5843=FACE_OUTER_BOUND ( 'NONE', #11818, .T. ) ;
#5856=VERTEX_POINT ( 'NONE', #12291 ) ;
#5903=CARTESIAN_POINT ( 'NONE',  ( -40.05918829504999934, -11.02709049255400053, 0.000000000000000000 ) ) ;
#5925=VERTEX_POINT ( 'NONE', #13256 ) ;
#5936=ORIENTED_EDGE ( 'NONE', *, *, #9864, .F. ) ;
#5948=EDGE_CURVE ( 'NONE', #7757, #8809, #10793, .T. ) ;
#5958=ORIENTED_EDGE ( 'NONE', *, *, #10035, .T. ) ;
#5959=EDGE_CURVE ( 'NONE', #12260, #7947, #4773, .T. ) ;
#5963=AXIS2_PLACEMENT_3D ( 'NONE', #10640, #5250, #5452 ) ;
#5970=DIRECTION ( 'NONE',  ( 0.000000000000000000, 0.000000000000000000, -1.000000000000000000 ) ) ;
#5977=CIRCLE ( 'NONE', #5526, 3.000000000000000000 ) ;
#6007=CARTESIAN_POINT ( 'NONE',  ( 1.940811704950003991, -6.027090492554000534, 0.000000000000000000 ) ) ;
#6024=CIRCLE ( 'NONE', #10724, 3.000000000000000000 ) ;
#6058=VECTOR ( 'NONE', #6823, 1000.000000000000000 ) ;
#6067=FACE_OUTER_BOUND ( 'NONE', #1210, .T. ) ;
#6141=LINE ( 'NONE', #7188, #2270 ) ;
#6150=DIRECTION ( 'NONE',  ( -0.000000000000000000, -0.000000000000000000, -1.000000000000000000 ) ) ;
#6169=ORIENTED_EDGE ( 'NONE', *, *, #279, .T. ) ;
#6190=ADVANCED_FACE ( 'NONE', ( #9549, #3413, #13729, #2161, #12824, #11579 ), #11716, .F. ) ;
#6196=CARTESIAN_POINT ( 'NONE',  ( -32.05918829504999934, -6.027090492554000534, 0.000000000000000000 ) ) ;
#6202=DIRECTION ( 'NONE',  ( -1.000000000000000000, 0.000000000000000000, 0.000000000000000000 ) ) ;
#6209=VERTEX_POINT ( 'NONE', #10664 ) ;
#6229=CIRCLE ( 'NONE', #1547, 18.50000000000000000 ) ;
#6243=CARTESIAN_POINT ( 'NONE',  ( -18.05918829504999934, 10.97290950744599947, 11.50000000000000000 ) ) ;
#6245=SHAPE_DEFINITION_REPRESENTATION ( #6352, #5062 ) ;
#6291=EDGE_CURVE ( 'NONE', #510, #13024, #8498, .T. ) ;
#6322=CARTESIAN_POINT ( 'NONE',  ( -35.05918829505000645, -6.027090492554000534, 10.00000000000000000 ) ) ;
#6352=PRODUCT_DEFINITION_SHAPE ( 'NONE', 'NONE',  #11074 ) ;
#6356=ORIENTED_EDGE ( 'NONE', *, *, #111, .T. ) ;
#6364=FACE_OUTER_BOUND ( 'NONE', #11533, .T. ) ;
#6388=DIRECTION ( 'NONE',  ( 1.000000000000000000, 0.000000000000000000, 0.000000000000000000 ) ) ;
#6434=AXIS2_PLACEMENT_3D ( 'NONE', #11654, #12825, #11856 ) ;
#6437=ADVANCED_FACE ( 'NONE', ( #11147 ), #5829, .F. ) ;
#6442=ORIENTED_EDGE ( 'NONE', *, *, #7709, .F. ) ;
#6461=DIRECTION ( 'NONE',  ( 1.000000000000000000, 0.000000000000000000, 0.000000000000000000 ) ) ;
#6462=DIRECTION ( 'NONE',  ( 1.000000000000000000, 0.000000000000000000, -0.000000000000000000 ) ) ;
#6484=CARTESIAN_POINT ( 'NONE',  ( -43.05918829505002066, 32.97290950744599769, 0.000000000000000000 ) ) ;
#6498=ORIENTED_EDGE ( 'NONE', *, *, #13216, .T. ) ;
#6532=CYLINDRICAL_SURFACE ( 'NONE', #1930, 6.049999999999999822 ) ;
#6539=CARTESIAN_POINT ( 'NONE',  ( -1.059188295049996231, -6.027090492554000534, 10.00000000000000000 ) ) ;
#6573=ORIENTED_EDGE ( 'NONE', *, *, #8428, .T. ) ;
#6583=LINE ( 'NONE', #9945, #8111 ) ;
#6610=LINE ( 'NONE', #2589, #896 ) ;
#6626=ORIENTED_EDGE ( 'NONE', *, *, #1375, .T. ) ;
#6664=AXIS2_PLACEMENT_3D ( 'NONE', #10325, #12414, #3012 ) ;
#6680=ORIENTED_EDGE ( 'NONE', *, *, #10227, .F. ) ;
#6681=CARTESIAN_POINT ( 'NONE',  ( 6.940811704950001548, 32.97290950744599769, 10.00000000000000000 ) ) ;
#6718=EDGE_CURVE ( 'NONE', #7472, #2002, #13159, .T. ) ;
#6730=ADVANCED_FACE ( 'NONE', ( #10937 ), #4572, .T. ) ;
#6747=VERTEX_POINT ( 'NONE', #11009 ) ;
#6749=DIRECTION ( 'NONE',  ( 1.000000000000000000, 0.000000000000000000, 0.000000000000000000 ) ) ;
#6797=ADVANCED_FACE ( 'NONE', ( #2634 ), #11069, .F. ) ;
#6802=EDGE_CURVE ( 'NONE', #5819, #9940, #7688, .T. ) ;
#6823=DIRECTION ( 'NONE',  ( -0.000000000000000000, -0.000000000000000000, -1.000000000000000000 ) ) ;
#6835=CARTESIAN_POINT ( 'NONE',  ( -18.05918829504999934, 10.97290950744599947, 0.000000000000000000 ) ) ;
#6845=ORIENTED_EDGE ( 'NONE', *, *, #4763, .T. ) ;
#6859=ADVANCED_FACE ( 'NONE', ( #156 ), #12945, .T. ) ;
#6864=ORIENTED_EDGE ( 'NONE', *, *, #2556, .T. ) ;
#6899=DIRECTION ( 'NONE',  ( 0.000000000000000000, -1.000000000000000000, 0.000000000000000000 ) ) ;
#6909=EDGE_CURVE ( 'NONE', #6747, #1393, #12297, .T. ) ;
#6914=AXIS2_PLACEMENT_3D ( 'NONE', #9013, #4895, #11253 ) ;
#6942=( LENGTH_UNIT ( ) NAMED_UNIT ( * ) SI_UNIT ( .MILLI., .METRE. ) );
#6974=CARTESIAN_POINT ( 'NONE',  ( -38.05918829505000645, 27.97290950744599769, 0.000000000000000000 ) ) ;
#6993=CARTESIAN_POINT ( 'NONE',  ( -24.10918829505000005, 10.97290950744599947, 0.000000000000000000 ) ) ;
#7018=ORIENTED_EDGE ( 'NONE', *, *, #11053, .T. ) ;
#7021=PLANE ( 'NONE',  #12008 ) ;
#7028=EDGE_CURVE ( 'NONE', #7612, #9617, #12254, .T. ) ;
#7037=DIRECTION ( 'NONE',  ( 1.000000000000000000, 0.000000000000000000, 0.000000000000000000 ) ) ;
#7042=DIRECTION ( 'NONE',  ( -1.000000000000000000, 0.000000000000000000, 0.000000000000000000 ) ) ;
#7058=ORIENTED_EDGE ( 'NONE', *, *, #669, .F. ) ;
#7083=CIRCLE ( 'NONE', #12456, 1.500000000000001332 ) ;
#7134=CARTESIAN_POINT ( 'NONE',  ( -4.059188295049996675, -6.027090492554000534, 0.000000000000000000 ) ) ;
#7179=FACE_OUTER_BOUND ( 'NONE', #13425, .T. ) ;
#7188=CARTESIAN_POINT ( 'NONE',  ( 3.940811704950003325, 35.97290950744599058, 10.00000000000000000 ) ) ;
#7207=CARTESIAN_POINT ( 'NONE',  ( -40.05918829505000645, 35.97290950744599058, 0.000000000000000000 ) ) ;
#7215=ORIENTED_EDGE ( 'NONE', *, *, #5516, .T. ) ;
#7239=ORIENTED_EDGE ( 'NONE', *, *, #12693, .T. ) ;
#7268=EDGE_CURVE ( 'NONE', #4017, #2836, #3510, .T. ) ;
#7272=DIRECTION ( 'NONE',  ( -0.000000000000000000, -0.000000000000000000, 1.000000000000000000 ) ) ;
#7327=CARTESIAN_POINT ( 'NONE',  ( -35.05918829504999934, 10.97290950744600124, 14.00000000000000000 ) ) ;
#7336=DIRECTION ( 'NONE',  ( 0.000000000000000000, -1.000000000000000000, 0.000000000000000000 ) ) ;
#7346=VECTOR ( 'NONE', #13209, 1000.000000000000000 ) ;
#7401=ORIENTED_EDGE ( 'NONE', *, *, #3002, .F. ) ;
#7412=DIRECTION ( 'NONE',  ( 1.000000000000000000, 0.000000000000000000, 0.000000000000000000 ) ) ;
#7419=FACE_OUTER_BOUND ( 'NONE', #11705, .T. ) ;
#7459=DIRECTION ( 'NONE',  ( 0.000000000000000000, 0.000000000000000000, 1.000000000000000000 ) ) ;
#7467=CARTESIAN_POINT ( 'NONE',  ( -12.00918829504999863, 10.97290950744599947, 0.000000000000000000 ) ) ;
#7472=VERTEX_POINT ( 'NONE', #9663 ) ;
#7474=DIRECTION ( 'NONE',  ( 0.000000000000000000, 0.000000000000000000, 1.000000000000000000 ) ) ;
#7483=DIRECTION ( 'NONE',  ( -1.000000000000000000, 0.000000000000000000, 0.000000000000000000 ) ) ;
#7543=DIRECTION ( 'NONE',  ( 1.000000000000000000, 0.000000000000000000, 0.000000000000000000 ) ) ;
#7551=ORIENTED_EDGE ( 'NONE', *, *, #3701, .F. ) ;
#7564=DIRECTION ( 'NONE',  ( 0.000000000000000000, 0.000000000000000000, 1.000000000000000000 ) ) ;
#7595=CARTESIAN_POINT ( 'NONE',  ( -35.05918829505000645, 27.97290950744599769, 10.00000000000000000 ) ) ;
#7597=DIRECTION ( 'NONE',  ( 0.000000000000000000, 0.000000000000000000, 1.000000000000000000 ) ) ;
#7612=VERTEX_POINT ( 'NONE', #11820 ) ;
#7633=FACE_BOUND ( 'NONE', #13054, .T. ) ;
#7688=LINE ( 'NONE', #7840, #4700 ) ;
#7696=DIRECTION ( 'NONE',  ( 1.000000000000000000, 0.000000000000000000, 0.000000000000000000 ) ) ;
#7707=AXIS2_PLACEMENT_3D ( 'NONE', #7595, #1324, #11882 ) ;
#7709=EDGE_CURVE ( 'NONE', #11194, #8213, #5296, .T. ) ;
#7716=DIRECTION ( 'NONE',  ( -0.000000000000000000, -0.000000000000000000, -1.000000000000000000 ) ) ;
#7736=VERTEX_POINT ( 'NONE', #551 ) ;
#7757=VERTEX_POINT ( 'NONE', #3645 ) ;
#7776=DIRECTION ( 'NONE',  ( 1.000000000000000000, 0.000000000000000000, 0.000000000000000000 ) ) ;
#7795=DIRECTION ( 'NONE',  ( -0.000000000000000000, -0.000000000000000000, 1.000000000000000000 ) ) ;
#7800=DIRECTION ( 'NONE',  ( 0.000000000000000000, 0.000000000000000000, -1.000000000000000000 ) ) ;
#7810=CARTESIAN_POINT ( 'NONE',  ( 3.940811704950003325, 32.97290950744599769, 0.000000000000000000 ) ) ;
#7835=EDGE_LOOP ( 'NONE', ( #1121, #3926 ) ) ;
#7840=CARTESIAN_POINT ( 'NONE',  ( -40.05918829504999934, -14.02709049255400053, 10.00000000000000000 ) ) ;
#7848=EDGE_LOOP ( 'NONE', ( #11911, #9020, #8120, #10652 ) ) ;
#7865=DIRECTION ( 'NONE',  ( 0.000000000000000000, 0.000000000000000000, 1.000000000000000000 ) ) ;
#7875=ORIENTED_EDGE ( 'NONE', *, *, #1500, .T. ) ;
#7881=ORIENTED_EDGE ( 'NONE', *, *, #9962, .F. ) ;
#7893=ORIENTED_EDGE ( 'NONE', *, *, #2548, .F. ) ;
#7910=ORIENTED_EDGE ( 'NONE', *, *, #13216, .F. ) ;
#7924=ORIENTED_EDGE ( 'NONE', *, *, #10739, .F. ) ;
#7947=VERTEX_POINT ( 'NONE', #8161 ) ;
#7949=CYLINDRICAL_SURFACE ( 'NONE', #10637, 3.000000000000002665 ) ;
#7950=LINE ( 'NONE', #6974, #5133 ) ;
#7962=ORIENTED_EDGE ( 'NONE', *, *, #12693, .F. ) ;
#7965=DIRECTION ( 'NONE',  ( -0.000000000000000000, -0.000000000000000000, 1.000000000000000000 ) ) ;
#7969=ORIENTED_EDGE ( 'NONE', *, *, #8517, .F. ) ;
#7979=VECTOR ( 'NONE', #2281, 1000.000000000000000 ) ;
#8012=CYLINDRICAL_SURFACE ( 'NONE', #2006, 2.999999999999998224 ) ;
#8019=ORIENTED_EDGE ( 'NONE', *, *, #4248, .F. ) ;
#8026=DIRECTION ( 'NONE',  ( -0.000000000000000000, -0.000000000000000000, 1.000000000000000000 ) ) ;
#8041=AXIS2_PLACEMENT_3D ( 'NONE', #4802, #13111, #5970 ) ;
#8043=FACE_BOUND ( 'NONE', #8887, .T. ) ;
#8047=DIRECTION ( 'NONE',  ( -0.000000000000000000, -0.000000000000000000, -1.000000000000000000 ) ) ;
#8079=EDGE_LOOP ( 'NONE', ( #7551, #10625, #7875, #6864 ) ) ;
#8083=FACE_OUTER_BOUND ( 'NONE', #1670, .T. ) ;
#8084=DIRECTION ( 'NONE',  ( 1.000000000000000000, 0.000000000000000000, 0.000000000000000000 ) ) ;
#8103=FACE_OUTER_BOUND ( 'NONE', #8974, .T. ) ;
#8109=EDGE_CURVE ( 'NONE', #68, #5925, #9715, .T. ) ;
#8111=VECTOR ( 'NONE', #2285, 1000.000000000000000 ) ;
#8120=ORIENTED_EDGE ( 'NONE', *, *, #6802, .F. ) ;
#8130=LINE ( 'NONE', #7207, #2672 ) ;
#8137=APPLICATION_CONTEXT ( 'automotive_design' ) ;
#8139=EDGE_CURVE ( 'NONE', #9940, #13024, #8922, .T. ) ;
#8161=CARTESIAN_POINT ( 'NONE',  ( -4.059188295049996675, 27.97290950744599769, 0.000000000000000000 ) ) ;
#8183=AXIS2_PLACEMENT_3D ( 'NONE', #1399, #3705, #496 ) ;
#8189=VECTOR ( 'NONE', #8289, 1000.000000000000000 ) ;
#8201=DIRECTION ( 'NONE',  ( 1.000000000000000000, 0.000000000000000000, 0.000000000000000000 ) ) ;
#8213=VERTEX_POINT ( 'NONE', #6681 ) ;
#8244=CIRCLE ( 'NONE', #4902, 20.00000000000000000 ) ;
#8289=DIRECTION ( 'NONE',  ( -0.000000000000000000, -0.000000000000000000, -1.000000000000000000 ) ) ;
#8290=AXIS2_PLACEMENT_3D ( 'NONE', #6243, #9325, #13578 ) ;
#8408=EDGE_CURVE ( 'NONE', #11490, #13362, #740, .T. ) ;
#8420=CARTESIAN_POINT ( 'NONE',  ( 3.940811704950003325, 35.97290950744599058, 10.00000000000000000 ) ) ;
#8428=EDGE_CURVE ( 'NONE', #6209, #1587, #5252, .T. ) ;
#8432=VECTOR ( 'NONE', #1556, 1000.000000000000000 ) ;
#8437=DIRECTION ( 'NONE',  ( 0.000000000000000000, 0.000000000000000000, 1.000000000000000000 ) ) ;
#8442=EDGE_CURVE ( 'NONE', #7612, #9088, #2608, .T. ) ;
#8462=VERTEX_POINT ( 'NONE', #2298 ) ;
#8469=CARTESIAN_POINT ( 'NONE',  ( -38.05918829504999934, 10.97290950744600124, 11.50000000000000000 ) ) ;
#8498=LINE ( 'NONE', #2307, #1561 ) ;
#8501=CIRCLE ( 'NONE', #4508, 3.000000000000002665 ) ;
#8502=ADVANCED_FACE ( 'NONE', ( #9535 ), #6532, .F. ) ;
#8517=EDGE_CURVE ( 'NONE', #2494, #1934, #3498, .T. ) ;
#8535=ORIENTED_EDGE ( 'NONE', *, *, #5041, .F. ) ;
#8536=ORIENTED_EDGE ( 'NONE', *, *, #13214, .T. ) ;
#8586=CARTESIAN_POINT ( 'NONE',  ( -12.00918829504999863, 10.97290950744599947, 0.000000000000000000 ) ) ;
#8610=LINE ( 'NONE', #4367, #12662 ) ;
#8680=EDGE_CURVE ( 'NONE', #2763, #11490, #9733, .T. ) ;
#8694=DIRECTION ( 'NONE',  ( 0.000000000000000000, 0.000000000000000000, 1.000000000000000000 ) ) ;
#8711=AXIS2_PLACEMENT_3D ( 'NONE', #10155, #8694, #1214 ) ;
#8713=AXIS2_PLACEMENT_3D ( 'NONE', #5903, #8854, #8084 ) ;
#8716=EDGE_LOOP ( 'NONE', ( #3558, #1889 ) ) ;
#8718=DIRECTION ( 'NONE',  ( 1.000000000000000000, 1.577021341797097560E-16, -0.000000000000000000 ) ) ;
#8728=VECTOR ( 'NONE', #12868, 1000.000000000000000 ) ;
#8748=ORIENTED_EDGE ( 'NONE', *, *, #11776, .T. ) ;
#8752=EDGE_LOOP ( 'NONE', ( #12589, #11249, #6169, #2604 ) ) ;
#8753=CARTESIAN_POINT ( 'NONE',  ( -4.059188295049996675, 27.97290950744599769, 0.000000000000000000 ) ) ;
#8758=CARTESIAN_POINT ( 'NONE',  ( -18.05918829504999934, 10.97290950744599947, 14.00000000000000000 ) ) ;
#8760=DIRECTION ( 'NONE',  ( -1.000000000000000000, 0.000000000000000000, 0.000000000000000000 ) ) ;
#8788=DIRECTION ( 'NONE',  ( 1.000000000000000000, 0.000000000000000000, 0.000000000000000000 ) ) ;
#8809=VERTEX_POINT ( 'NONE', #11529 ) ;
#8829=LINE ( 'NONE', #6007, #4828 ) ;
#8854=DIRECTION ( 'NONE',  ( 0.000000000000000000, 0.000000000000000000, 1.000000000000000000 ) ) ;
#8887=EDGE_LOOP ( 'NONE', ( #6498, #7239 ) ) ;
#8893=CARTESIAN_POINT ( 'NONE',  ( 0.4408117049500004381, 10.97290950744600124, 12.50000000000000000 ) ) ;
#8919=EDGE_CURVE ( 'NONE', #5925, #68, #2399, .T. ) ;
#8922=LINE ( 'NONE', #4532, #10842 ) ;
#8974=EDGE_LOOP ( 'NONE', ( #2977, #3113, #1506, #7962 ) ) ;
#9013=CARTESIAN_POINT ( 'NONE',  ( -1.059188295049996231, 27.97290950744599769, 0.000000000000000000 ) ) ;
#9015=EDGE_CURVE ( 'NONE', #13437, #5856, #11974, .T. ) ;
#9018=ADVANCED_FACE ( 'NONE', ( #1607 ), #5715, .F. ) ;
#9020=ORIENTED_EDGE ( 'NONE', *, *, #8139, .F. ) ;
#9031=DIRECTION ( 'NONE',  ( 1.000000000000000000, 0.000000000000000000, 0.000000000000000000 ) ) ;
#9041=ADVANCED_FACE ( 'NONE', ( #12367 ), #7949, .F. ) ;
#9048=DIRECTION ( 'NONE',  ( 1.000000000000000000, 0.000000000000000000, 0.000000000000000000 ) ) ;
#9084=ADVANCED_FACE ( 'NONE', ( #8103 ), #354, .F. ) ;
#9088=VERTEX_POINT ( 'NONE', #4756 ) ;
#9098=CIRCLE ( 'NONE', #13119, 2.999999999999999112 ) ;
#9113=EDGE_CURVE ( 'NONE', #755, #8462, #11522, .T. ) ;
#9229=CARTESIAN_POINT ( 'NONE',  ( 6.940811704950001548, 32.97290950744599769, 0.000000000000000000 ) ) ;
#9251=ORIENTED_EDGE ( 'NONE', *, *, #9113, .T. ) ;
#9254=ORIENTED_EDGE ( 'NONE', *, *, #2548, .T. ) ;
#9255=CARTESIAN_POINT ( 'NONE',  ( 3.940811704950009542, -14.02709049255400053, 10.00000000000000000 ) ) ;
#9267=DIRECTION ( 'NONE',  ( -0.000000000000000000, -0.000000000000000000, -1.000000000000000000 ) ) ;
#9278=CARTESIAN_POINT ( 'NONE',  ( 6.940811704950009542, -11.02709049255400053, 0.000000000000000000 ) ) ;
#9294=CARTESIAN_POINT ( 'NONE',  ( -24.10918829505000005, 10.97290950744599947, 14.00000000000000000 ) ) ;
#9325=DIRECTION ( 'NONE',  ( 0.000000000000000000, 0.000000000000000000, 1.000000000000000000 ) ) ;
#9334=LINE ( 'NONE', #4035, #8189 ) ;
#9342=DIRECTION ( 'NONE',  ( -0.000000000000000000, -0.000000000000000000, 1.000000000000000000 ) ) ;
#9383=CARTESIAN_POINT ( 'NONE',  ( -40.05918829504999934, -14.02709049255400053, 10.00000000000000000 ) ) ;
#9384=AXIS2_PLACEMENT_3D ( 'NONE', #11907, #2358, #3527 ) ;
#9398=CARTESIAN_POINT ( 'NONE',  ( -18.05918829504999934, 10.97290950744599947, 0.000000000000000000 ) ) ;
#9467=DIRECTION ( 'NONE',  ( -1.000000000000000000, -0.000000000000000000, -0.000000000000000000 ) ) ;
#9474=DIRECTION ( 'NONE',  ( 1.000000000000000000, 0.000000000000000000, 0.000000000000000000 ) ) ;
#9487=DIRECTION ( 'NONE',  ( 0.000000000000000000, 0.000000000000000000, 1.000000000000000000 ) ) ;
#9505=ORIENTED_EDGE ( 'NONE', *, *, #11455, .T. ) ;
#9535=FACE_OUTER_BOUND ( 'NONE', #5515, .T. ) ;
#9538=CIRCLE ( 'NONE', #10434, 6.049999999999999822 ) ;
#9549=FACE_BOUND ( 'NONE', #1034, .T. ) ;
#9554=AXIS2_PLACEMENT_3D ( 'NONE', #4962, #10340, #6202 ) ;
#9572=DIRECTION ( 'NONE',  ( -1.182766006347823109E-16, 1.000000000000000000, -0.000000000000000000 ) ) ;
#9574=ORIENTED_EDGE ( 'NONE', *, *, #296, .T. ) ;
#9616=VECTOR ( 'NONE', #12001, 1000.000000000000000 ) ;
#9617=VERTEX_POINT ( 'NONE', #11918 ) ;
#9633=CARTESIAN_POINT ( 'NONE',  ( -35.05918829505000645, 27.97290950744599769, 10.00000000000000000 ) ) ;
#9649=VERTEX_POINT ( 'NONE', #8420 ) ;
#9655=FACE_OUTER_BOUND ( 'NONE', #3452, .T. ) ;
#9663=CARTESIAN_POINT ( 'NONE',  ( -4.059188295049996675, 27.97290950744599769, 10.00000000000000000 ) ) ;
#9677=PRODUCT_CONTEXT ( 'NONE', #8137, 'mechanical' ) ;
#9681=DIRECTION ( 'NONE',  ( -0.000000000000000000, -0.000000000000000000, 1.000000000000000000 ) ) ;
#9695=ORIENTED_EDGE ( 'NONE', *, *, #9015, .F. ) ;
#9709=EDGE_CURVE ( 'NONE', #5576, #7736, #10220, .T. ) ;
#9715=CIRCLE ( 'NONE', #361, 3.000000000000002665 ) ;
#9718=DIRECTION ( 'NONE',  ( -0.000000000000000000, -0.000000000000000000, 1.000000000000000000 ) ) ;
#9733=CIRCLE ( 'NONE', #2615, 6.049999999999999822 ) ;
#9734=CARTESIAN_POINT ( 'NONE',  ( -36.55918829504999934, 10.97290950744599947, 14.00000000000000000 ) ) ;
#9743=CARTESIAN_POINT ( 'NONE',  ( -18.05918829504999934, 10.97290950744599947, 0.000000000000000000 ) ) ;
#9762=MANIFOLD_SOLID_BREP ( 'Cut-Extrude3', #11491 ) ;
#9776=AXIS2_PLACEMENT_3D ( 'NONE', #3545, #2513, #6749 ) ;
#9791=CARTESIAN_POINT ( 'NONE',  ( -32.05918829504999934, 27.97290950744599769, 0.000000000000000000 ) ) ;
#9792=ADVANCED_FACE ( 'NONE', ( #11016 ), #11077, .F. ) ;
#9818=CARTESIAN_POINT ( 'NONE',  ( -40.05918829505000645, 32.97290950744599769, 10.00000000000000000 ) ) ;
#9864=EDGE_CURVE ( 'NONE', #5856, #6747, #8130, .T. ) ;
#9876=ORIENTED_EDGE ( 'NONE', *, *, #11377, .F. ) ;
#9887=ORIENTED_EDGE ( 'NONE', *, *, #13801, .T. ) ;
#9940=VERTEX_POINT ( 'NONE', #9255 ) ;
#9945=CARTESIAN_POINT ( 'NONE',  ( 6.940811704950009542, -11.02709049255400053, 10.00000000000000000 ) ) ;
#9947=DIRECTION ( 'NONE',  ( -0.000000000000000000, -0.000000000000000000, -1.000000000000000000 ) ) ;
#9954=EDGE_LOOP ( 'NONE', ( #1557, #6680, #367, #4001 ) ) ;
#9956=SURFACE_STYLE_USAGE ( .BOTH. , #3738 ) ;
#9962=EDGE_CURVE ( 'NONE', #11490, #2763, #5303, .T. ) ;
#9988=EDGE_CURVE ( 'NONE', #7736, #10331, #7083, .T. ) ;
#10035=EDGE_CURVE ( 'NONE', #4386, #4017, #5093, .T. ) ;
#10070=DIRECTION ( 'NONE',  ( 1.000000000000000000, 0.000000000000000000, 0.000000000000000000 ) ) ;
#10103=CIRCLE ( 'NONE', #1846, 3.000000000000000000 ) ;
#10106=DIRECTION ( 'NONE',  ( 1.000000000000000000, 0.000000000000000000, 0.000000000000000000 ) ) ;
#10112=CARTESIAN_POINT ( 'NONE',  ( -43.05918829505002066, 32.97290950744599769, 10.00000000000000000 ) ) ;
#10114=DIRECTION ( 'NONE',  ( -0.000000000000000000, -0.000000000000000000, 1.000000000000000000 ) ) ;
#10126=FACE_OUTER_BOUND ( 'NONE', #7848, .T. ) ;
#10128=DIRECTION ( 'NONE',  ( -1.000000000000000000, 0.000000000000000000, 0.000000000000000000 ) ) ;
#10131=DIRECTION ( 'NONE',  ( 1.000000000000000000, 0.000000000000000000, 0.000000000000000000 ) ) ;
#10139=DIRECTION ( 'NONE',  ( -0.000000000000000000, -0.000000000000000000, 1.000000000000000000 ) ) ;
#10155=CARTESIAN_POINT ( 'NONE',  ( -18.05918829504999934, 10.97290950744599947, 14.00000000000000000 ) ) ;
#10162=DIRECTION ( 'NONE',  ( -1.000000000000000000, 0.000000000000000000, 0.000000000000000000 ) ) ;
#10170=EDGE_LOOP ( 'NONE', ( #11316, #12121, #638, #11480 ) ) ;
#10179=ORIENTED_EDGE ( 'NONE', *, *, #14, .F. ) ;
#10220=CIRCLE ( 'NONE', #5294, 18.50000000000000000 ) ;
#10226=CARTESIAN_POINT ( 'NONE',  ( -38.05918829504999934, 10.97290950744600124, 10.00000000000000000 ) ) ;
#10227=EDGE_CURVE ( 'NONE', #2836, #10499, #13148, .T. ) ;
#10258=DIRECTION ( 'NONE',  ( 1.000000000000000000, 0.000000000000000000, 0.000000000000000000 ) ) ;
#10296=LINE ( 'NONE', #12448, #12905 ) ;
#10315=EDGE_CURVE ( 'NONE', #5819, #510, #10296, .T. ) ;
#10325=CARTESIAN_POINT ( 'NONE',  ( -35.05918829504999934, 10.97290950744600124, 12.50000000000000000 ) ) ;
#10331=VERTEX_POINT ( 'NONE', #10226 ) ;
#10340=DIRECTION ( 'NONE',  ( -0.000000000000000000, -0.000000000000000000, -1.000000000000000000 ) ) ;
#10352=ORIENTED_EDGE ( 'NONE', *, *, #1375, .F. ) ;
#10357=DIRECTION ( 'NONE',  ( 1.000000000000000000, 0.000000000000000000, 0.000000000000000000 ) ) ;
#10358=DIRECTION ( 'NONE',  ( 0.000000000000000000, 0.000000000000000000, 1.000000000000000000 ) ) ;
#10416=EDGE_LOOP ( 'NONE', ( #6573, #2059, #2531, #13126 ) ) ;
#10434=AXIS2_PLACEMENT_3D ( 'NONE', #8758, #3781, #7042 ) ;
#10454=CARTESIAN_POINT ( 'NONE',  ( -32.05918829504999934, -6.027090492554000534, 0.000000000000000000 ) ) ;
#10470=PRODUCT_DEFINITION_FORMATION_WITH_SPECIFIED_SOURCE ( 'ANY', '', #463, .NOT_KNOWN. ) ;
#10477=AXIS2_PLACEMENT_3D ( 'NONE', #5335, #11766, #6462 ) ;
#10492=ORIENTED_EDGE ( 'NONE', *, *, #9113, .F. ) ;
#10499=VERTEX_POINT ( 'NONE', #1114 ) ;
#10502=CIRCLE ( 'NONE', #13623, 3.000000000000000000 ) ;
#10508=ADVANCED_FACE ( 'NONE', ( #9655 ), #11136, .F. ) ;
#10538=CARTESIAN_POINT ( 'NONE',  ( -40.05918829504999934, -11.02709049255400053, 0.000000000000000000 ) ) ;
#10575=DIRECTION ( 'NONE',  ( 0.000000000000000000, 0.000000000000000000, 1.000000000000000000 ) ) ;
#10625=ORIENTED_EDGE ( 'NONE', *, *, #3002, .T. ) ;
#10637=AXIS2_PLACEMENT_3D ( 'NONE', #12303, #8026, #11177 ) ;
#10640=CARTESIAN_POINT ( 'NONE',  ( -40.05918829505000645, 32.97290950744599769, 10.00000000000000000 ) ) ;
#10650=ORIENTED_EDGE ( 'NONE', *, *, #279, .F. ) ;
#10652=ORIENTED_EDGE ( 'NONE', *, *, #10315, .T. ) ;
#10658=ADVANCED_FACE ( 'NONE', ( #5843 ), #8012, .T. ) ;
#10664=CARTESIAN_POINT ( 'NONE',  ( -36.55918829504999934, 10.97290950744599947, 12.50000000000000000 ) ) ;
#10692=ORIENTED_EDGE ( 'NONE', *, *, #2138, .T. ) ;
#10724=AXIS2_PLACEMENT_3D ( 'NONE', #3366, #7597, #11883 ) ;
#10739=EDGE_CURVE ( 'NONE', #6209, #1934, #12474, .T. ) ;
#10748=EDGE_LOOP ( 'NONE', ( #2386, #7893 ) ) ;
#10769=LINE ( 'NONE', #9791, #645 ) ;
#10777=ORIENTED_EDGE ( 'NONE', *, *, #9864, .T. ) ;
#10784=DIRECTION ( 'NONE',  ( 1.000000000000000000, 0.000000000000000000, 0.000000000000000000 ) ) ;
#10793=CIRCLE ( 'NONE', #2559, 3.000000000000002665 ) ;
#10811=DIRECTION ( 'NONE',  ( 1.000000000000000000, 0.000000000000000000, 0.000000000000000000 ) ) ;
#10842=VECTOR ( 'NONE', #3629, 1000.000000000000000 ) ;
#10875=FACE_OUTER_BOUND ( 'NONE', #3824, .T. ) ;
#10891=CARTESIAN_POINT ( 'NONE',  ( -38.05918829505000645, -6.027090492554000534, 0.000000000000000000 ) ) ;
#10903=ORIENTED_EDGE ( 'NONE', *, *, #4829, .T. ) ;
#10908=LINE ( 'NONE', #8586, #12936 ) ;
#10937=FACE_OUTER_BOUND ( 'NONE', #10416, .T. ) ;
#10959=CIRCLE ( 'NONE', #908, 3.000000000000002665 ) ;
#10987=EDGE_LOOP ( 'NONE', ( #9251, #12783 ) ) ;
#11009=CARTESIAN_POINT ( 'NONE',  ( -40.05918829505000645, 35.97290950744599769, 0.000000000000000000 ) ) ;
#11016=FACE_OUTER_BOUND ( 'NONE', #2312, .T. ) ;
#11053=EDGE_CURVE ( 'NONE', #13024, #13765, #9098, .T. ) ;
#11059=ORIENTED_EDGE ( 'NONE', *, *, #9988, .T. ) ;
#11068=AXIS2_PLACEMENT_3D ( 'NONE', #1716, #9267, #6461 ) ;
#11069=CYLINDRICAL_SURFACE ( 'NONE', #9384, 3.000000000000002665 ) ;
#11074=PRODUCT_DEFINITION ( 'UNKNOWN', '', #10470, #13527 ) ;
#11077=CYLINDRICAL_SURFACE ( 'NONE', #831, 3.000000000000000000 ) ;
#11127=ORIENTED_EDGE ( 'NONE', *, *, #7268, .T. ) ;
#11130=CARTESIAN_POINT ( 'NONE',  ( -43.05918829505001355, -11.02709049255400053, 10.00000000000000000 ) ) ;
#11136=TOROIDAL_SURFACE ( 'NONE', #864, 20.00000000000000000, 1.500000000000000000 ) ;
#11147=FACE_OUTER_BOUND ( 'NONE', #1135, .T. ) ;
#11157=DIRECTION ( 'NONE',  ( 0.000000000000000000, 1.000000000000000000, 0.000000000000000000 ) ) ;
#11177=DIRECTION ( 'NONE',  ( 1.000000000000000000, 0.000000000000000000, 0.000000000000000000 ) ) ;
#11182=VECTOR ( 'NONE', #4943, 1000.000000000000000 ) ;
#11194=VERTEX_POINT ( 'NONE', #11547 ) ;
#11217=( NAMED_UNIT ( * ) PLANE_ANGLE_UNIT ( ) SI_UNIT ( $, .RADIAN. ) );
#11239=CARTESIAN_POINT ( 'NONE',  ( -35.05918829505000645, 27.97290950744599769, 0.000000000000000000 ) ) ;
#11249=ORIENTED_EDGE ( 'NONE', *, *, #559, .F. ) ;
#11253=DIRECTION ( 'NONE',  ( 1.000000000000000000, 0.000000000000000000, 0.000000000000000000 ) ) ;
#11271=CYLINDRICAL_SURFACE ( 'NONE', #4321, 18.50000000000000000 ) ;
#11291=CARTESIAN_POINT ( 'NONE',  ( -24.10918829505000005, 10.97290950744599947, 0.000000000000000000 ) ) ;
#11296=DIRECTION ( 'NONE',  ( 0.000000000000000000, -0.000000000000000000, -1.000000000000000000 ) ) ;
#11297=DIRECTION ( 'NONE',  ( 0.000000000000000000, -0.000000000000000000, 1.000000000000000000 ) ) ;
#11302=ADVANCED_FACE ( 'NONE', ( #8083 ), #7021, .F. ) ;
#11316=ORIENTED_EDGE ( 'NONE', *, *, #13801, .F. ) ;
#11323=ORIENTED_EDGE ( 'NONE', *, *, #11053, .F. ) ;
#11337=DIRECTION ( 'NONE',  ( -0.000000000000000000, -0.000000000000000000, -1.000000000000000000 ) ) ;
#11365=DIRECTION ( 'NONE',  ( 0.000000000000000000, 0.000000000000000000, 1.000000000000000000 ) ) ;
#11377=EDGE_CURVE ( 'NONE', #7947, #7472, #1346, .T. ) ;
#11430=ORIENTED_EDGE ( 'NONE', *, *, #489, .F. ) ;
#11435=LINE ( 'NONE', #10454, #11182 ) ;
#11455=EDGE_CURVE ( 'NONE', #9940, #11194, #2669, .T. ) ;
#11480=ORIENTED_EDGE ( 'NONE', *, *, #2138, .F. ) ;
#11490=VERTEX_POINT ( 'NONE', #6993 ) ;
#11491=CLOSED_SHELL ( 'NONE', ( #2655, #11863, #6730, #9792, #6797, #9041, #9018, #8502, #12189, #1036, #12136, #11599, #10658, #11302, #6859, #3639, #186, #6190, #9084, #663, #6437, #13088, #13150, #5626, #4167, #12882, #10508 ) ) ;
#11522=CIRCLE ( 'NONE', #13531, 3.000000000000002665 ) ;
#11529=CARTESIAN_POINT ( 'NONE',  ( -38.05918829505000645, 27.97290950744599769, 0.000000000000000000 ) ) ;
#11532=DIRECTION ( 'NONE',  ( 1.000000000000000000, 0.000000000000000000, 0.000000000000000000 ) ) ;
#11533=EDGE_LOOP ( 'NONE', ( #13124, #4330, #7969, #11932 ) ) ;
#11547=CARTESIAN_POINT ( 'NONE',  ( 6.940811704950009542, -11.02709049255400053, 10.00000000000000000 ) ) ;
#11579=FACE_OUTER_BOUND ( 'NONE', #5436, .T. ) ;
#11599=ADVANCED_FACE ( 'NONE', ( #13492 ), #5110, .F. ) ;
#11630=CARTESIAN_POINT ( 'NONE',  ( -35.05918829505000645, -6.027090492554000534, 0.000000000000000000 ) ) ;
#11635=ORIENTED_EDGE ( 'NONE', *, *, #3826, .F. ) ;
#11654=CARTESIAN_POINT ( 'NONE',  ( 0.000000000000000000, 0.000000000000000000, 0.000000000000000000 ) ) ;
#11666=DIRECTION ( 'NONE',  ( 1.000000000000000000, 0.000000000000000000, 0.000000000000000000 ) ) ;
#11699=CARTESIAN_POINT ( 'NONE',  ( -43.05918829505001355, -11.02709049255400053, 10.00000000000000000 ) ) ;
#11705=EDGE_LOOP ( 'NONE', ( #6356, #2335, #9505, #4560, #6626, #3457, #5958, #11127 ) ) ;
#11708=PLANE ( 'NONE',  #10477 ) ;
#11716=PLANE ( 'NONE',  #445 ) ;
#11728=UNCERTAINTY_MEASURE_WITH_UNIT (LENGTH_MEASURE( 1.000000000000000082E-05 ), #6942, 'distance_accuracy_value', 'NONE');
#11737=ORIENTED_EDGE ( 'NONE', *, *, #3826, .T. ) ;
#11765=AXIS2_PLACEMENT_3D ( 'NONE', #11630, #7272, #5197 ) ;
#11766=DIRECTION ( 'NONE',  ( 0.000000000000000000, 0.000000000000000000, 1.000000000000000000 ) ) ;
#11770=STYLED_ITEM ( 'NONE', ( #12124 ), #9762 ) ;
#11776=EDGE_CURVE ( 'NONE', #7757, #68, #10769, .T. ) ;
#11806=EDGE_LOOP ( 'NONE', ( #1043, #733 ) ) ;
#11818=EDGE_LOOP ( 'NONE', ( #5206, #1280, #10352, #12123 ) ) ;
#11820=CARTESIAN_POINT ( 'NONE',  ( -4.059188295049996675, -6.027090492554000534, 0.000000000000000000 ) ) ;
#11840=ORIENTED_EDGE ( 'NONE', *, *, #5959, .F. ) ;
#11856=DIRECTION ( 'NONE',  ( 1.000000000000000000, 0.000000000000000000, 0.000000000000000000 ) ) ;
#11863=ADVANCED_FACE ( 'NONE', ( #6364 ), #5318, .T. ) ;
#11882=DIRECTION ( 'NONE',  ( 1.000000000000000000, 0.000000000000000000, 0.000000000000000000 ) ) ;
#11883=DIRECTION ( 'NONE',  ( 1.000000000000000000, 0.000000000000000000, 0.000000000000000000 ) ) ;
#11907=CARTESIAN_POINT ( 'NONE',  ( -35.05918829505000645, -6.027090492554000534, 0.000000000000000000 ) ) ;
#11911=ORIENTED_EDGE ( 'NONE', *, *, #6291, .T. ) ;
#11914=FACE_BOUND ( 'NONE', #4416, .T. ) ;
#11918=CARTESIAN_POINT ( 'NONE',  ( -4.059188295049996675, -6.027090492554000534, 10.00000000000000000 ) ) ;
#11932=ORIENTED_EDGE ( 'NONE', *, *, #13612, .F. ) ;
#11939=CYLINDRICAL_SURFACE ( 'NONE', #854, 3.000000000000002665 ) ;
#11974=CIRCLE ( 'NONE', #2629, 2.999999999999998224 ) ;
#11993=AXIS2_PLACEMENT_3D ( 'NONE', #2010, #4158, #7543 ) ;
#11994=( GEOMETRIC_REPRESENTATION_CONTEXT ( 3 ) GLOBAL_UNCERTAINTY_ASSIGNED_CONTEXT ( ( #11728 ) ) GLOBAL_UNIT_ASSIGNED_CONTEXT ( ( #6942, #11217, #3470 ) ) REPRESENTATION_CONTEXT ( 'NONE', 'WORKASPACE' ) );
#12001=DIRECTION ( 'NONE',  ( 1.577021341797097560E-16, -1.000000000000000000, 0.000000000000000000 ) ) ;
#12008=AXIS2_PLACEMENT_3D ( 'NONE', #12667, #7336, #11296 ) ;
#12043=DIRECTION ( 'NONE',  ( 1.000000000000000000, 0.000000000000000000, 0.000000000000000000 ) ) ;
#12058=AXIS2_PLACEMENT_3D ( 'NONE', #12278, #11365, #10258 ) ;
#12068=PLANE ( 'NONE',  #13387 ) ;
#12086=EDGE_LOOP ( 'NONE', ( #4220, #9887 ) ) ;
#12121=ORIENTED_EDGE ( 'NONE', *, *, #11377, .T. ) ;
#12123=ORIENTED_EDGE ( 'NONE', *, *, #14, .T. ) ;
#12124=PRESENTATION_STYLE_ASSIGNMENT (( #9956 ) ) ;
#12136=ADVANCED_FACE ( 'NONE', ( #6067 ), #3030, .T. ) ;
#12189=ADVANCED_FACE ( 'NONE', ( #7179 ), #11939, .T. ) ;
#12215=CARTESIAN_POINT ( 'NONE',  ( -1.059188295050000894, 10.97290950744599947, 12.50000000000000000 ) ) ;
#12219=ORIENTED_EDGE ( 'NONE', *, *, #10035, .F. ) ;
#12246=CARTESIAN_POINT ( 'NONE',  ( -35.05918829505000645, -6.027090492554000534, 0.000000000000000000 ) ) ;
#12254=LINE ( 'NONE', #7134, #5802 ) ;
#12260=VERTEX_POINT ( 'NONE', #2249 ) ;
#12278=CARTESIAN_POINT ( 'NONE',  ( -1.059188295049996231, -6.027090492554000534, 10.00000000000000000 ) ) ;
#12291=CARTESIAN_POINT ( 'NONE',  ( 3.940811704950003325, 35.97290950744599058, 0.000000000000000000 ) ) ;
#12296=CIRCLE ( 'NONE', #8041, 1.499999999999999556 ) ;
#12297=CIRCLE ( 'NONE', #3597, 3.000000000000002665 ) ;
#12303=CARTESIAN_POINT ( 'NONE',  ( -35.05918829505000645, 27.97290950744599769, 0.000000000000000000 ) ) ;
#12319=EDGE_LOOP ( 'NONE', ( #9876, #11840, #10692, #5443 ) ) ;
#12321=LINE ( 'NONE', #1622, #1461 ) ;
#12323=FACE_OUTER_BOUND ( 'NONE', #13275, .T. ) ;
#12347=ORIENTED_EDGE ( 'NONE', *, *, #1207, .T. ) ;
#12367=FACE_OUTER_BOUND ( 'NONE', #12370, .T. ) ;
#12370=EDGE_LOOP ( 'NONE', ( #2481, #4125, #201, #619 ) ) ;
#12388=FACE_OUTER_BOUND ( 'NONE', #8079, .T. ) ;
#12395=ORIENTED_EDGE ( 'NONE', *, *, #8442, .F. ) ;
#12414=DIRECTION ( 'NONE',  ( 1.224646799147353207E-16, 1.000000000000000000, -0.000000000000000000 ) ) ;
#12440=ORIENTED_EDGE ( 'NONE', *, *, #559, .T. ) ;
#12444=CARTESIAN_POINT ( 'NONE',  ( -1.059188295049996231, 27.97290950744599769, 10.00000000000000000 ) ) ;
#12448=CARTESIAN_POINT ( 'NONE',  ( -40.05918829504999934, -14.02709049255400053, 10.00000000000000000 ) ) ;
#12456=AXIS2_PLACEMENT_3D ( 'NONE', #8469, #1002, #4299 ) ;
#12474=CIRCLE ( 'NONE', #6664, 1.500000000000001332 ) ;
#12524=ORIENTED_EDGE ( 'NONE', *, *, #7028, .T. ) ;
#12589=ORIENTED_EDGE ( 'NONE', *, *, #7028, .F. ) ;
#12603=CARTESIAN_POINT ( 'NONE',  ( 3.940811704950003325, 32.97290950744599769, 10.00000000000000000 ) ) ;
#12605=FACE_OUTER_BOUND ( 'NONE', #13703, .T. ) ;
#12606=DIRECTION ( 'NONE',  ( 0.000000000000000000, 0.000000000000000000, 1.000000000000000000 ) ) ;
#12617=ORIENTED_EDGE ( 'NONE', *, *, #1060, .F. ) ;
#12641=CARTESIAN_POINT ( 'NONE',  ( -35.05918829505000645, 27.97290950744599769, 0.000000000000000000 ) ) ;
#12657=DIRECTION ( 'NONE',  ( 0.000000000000000000, 0.000000000000000000, 1.000000000000000000 ) ) ;
#12662=VECTOR ( 'NONE', #9467, 1000.000000000000000 ) ;
#12667=CARTESIAN_POINT ( 'NONE',  ( -40.05918829505000645, 35.97290950744599058, 10.00000000000000000 ) ) ;
#12683=CARTESIAN_POINT ( 'NONE',  ( -18.05918829504999934, 10.97290950744599947, 14.00000000000000000 ) ) ;
#12693=EDGE_CURVE ( 'NONE', #13362, #3609, #3552, .T. ) ;
#12724=CARTESIAN_POINT ( 'NONE',  ( -40.05918829505000645, 35.97290950744599769, 10.00000000000000000 ) ) ;
#12746=DIRECTION ( 'NONE',  ( 0.000000000000000000, 0.000000000000000000, 1.000000000000000000 ) ) ;
#12751=AXIS2_PLACEMENT_3D ( 'NONE', #12603, #2008, #726 ) ;
#12757=FACE_BOUND ( 'NONE', #246, .T. ) ;
#12776=LINE ( 'NONE', #6484, #9616 ) ;
#12783=ORIENTED_EDGE ( 'NONE', *, *, #1611, .T. ) ;
#12790=CARTESIAN_POINT ( 'NONE',  ( -18.05918829504999934, 10.97290950744599947, 12.50000000000000000 ) ) ;
#12810=ORIENTED_EDGE ( 'NONE', *, *, #13134, .F. ) ;
#12824=FACE_BOUND ( 'NONE', #7835, .T. ) ;
#12825=DIRECTION ( 'NONE',  ( 0.000000000000000000, 0.000000000000000000, 1.000000000000000000 ) ) ;
#12868=DIRECTION ( 'NONE',  ( -0.000000000000000000, -0.000000000000000000, -1.000000000000000000 ) ) ;
#12876=EDGE_CURVE ( 'NONE', #4017, #1393, #5827, .T. ) ;
#12882=ADVANCED_FACE ( 'NONE', ( #10875 ), #1505, .T. ) ;
#12905=VECTOR ( 'NONE', #8047, 1000.000000000000000 ) ;
#12936=VECTOR ( 'NONE', #4478, 1000.000000000000000 ) ;
#12945=CYLINDRICAL_SURFACE ( 'NONE', #13604, 3.000000000000002665 ) ;
#12968=AXIS2_PLACEMENT_3D ( 'NONE', #12246, #4714, #9031 ) ;
#12983=VECTOR ( 'NONE', #7795, 1000.000000000000000 ) ;
#13001=ORIENTED_EDGE ( 'NONE', *, *, #8517, .T. ) ;
#13002=ORIENTED_EDGE ( 'NONE', *, *, #1611, .F. ) ;
#13023=CARTESIAN_POINT ( 'NONE',  ( -18.05918829504999934, 10.97290950744599947, 0.000000000000000000 ) ) ;
#13024=VERTEX_POINT ( 'NONE', #3951 ) ;
#13033=CARTESIAN_POINT ( 'NONE',  ( -35.05918829505000645, 27.97290950744599769, 0.000000000000000000 ) ) ;
#13054=EDGE_LOOP ( 'NONE', ( #4846, #720 ) ) ;
#13088=ADVANCED_FACE ( 'NONE', ( #12605 ), #2142, .F. ) ;
#13103=MECHANICAL_DESIGN_GEOMETRIC_PRESENTATION_REPRESENTATION('',(#11770),#11994);
#13111=DIRECTION ( 'NONE',  ( 0.000000000000000000, -1.000000000000000000, 0.000000000000000000 ) ) ;
#13119=AXIS2_PLACEMENT_3D ( 'NONE', #13186, #7865, #8788 ) ;
#13124=ORIENTED_EDGE ( 'NONE', *, *, #8428, .F. ) ;
#13126=ORIENTED_EDGE ( 'NONE', *, *, #1500, .F. ) ;
#13134=EDGE_CURVE ( 'NONE', #9649, #4386, #8610, .T. ) ;
#13148=LINE ( 'NONE', #11130, #8432 ) ;
#13150=ADVANCED_FACE ( 'NONE', ( #1068 ), #3315, .F. ) ;
#13156=CARTESIAN_POINT ( 'NONE',  ( -18.05918829504999934, 10.97290950744599947, 14.00000000000000000 ) ) ;
#13159=CIRCLE ( 'NONE', #4032, 3.000000000000000000 ) ;
#13186=CARTESIAN_POINT ( 'NONE',  ( 3.940811704950010430, -11.02709049255400053, 0.000000000000000000 ) ) ;
#13209=DIRECTION ( 'NONE',  ( 1.577021341797097560E-16, -1.000000000000000000, 0.000000000000000000 ) ) ;
#13214=EDGE_CURVE ( 'NONE', #1934, #2494, #2195, .T. ) ;
#13216=EDGE_CURVE ( 'NONE', #3609, #13362, #9538, .T. ) ;
#13238=DIRECTION ( 'NONE',  ( -0.000000000000000000, -0.000000000000000000, 1.000000000000000000 ) ) ;
#13256=CARTESIAN_POINT ( 'NONE',  ( -38.05918829505000645, 27.97290950744599769, 10.00000000000000000 ) ) ;
#13270=DIRECTION ( 'NONE',  ( 1.000000000000000000, 0.000000000000000000, 0.000000000000000000 ) ) ;
#13275=EDGE_LOOP ( 'NONE', ( #13001, #8536 ) ) ;
#13289=CARTESIAN_POINT ( 'NONE',  ( 0.4408117049500004381, 10.97290950744600124, 11.50000000000000000 ) ) ;
#13292=VECTOR ( 'NONE', #4999, 1000.000000000000000 ) ;
#13299=FILL_AREA_STYLE ('',( #3540 ) ) ;
#13362=VERTEX_POINT ( 'NONE', #9294 ) ;
#13387=AXIS2_PLACEMENT_3D ( 'NONE', #2387, #8718, #4740 ) ;
#13425=EDGE_LOOP ( 'NONE', ( #13790, #4166, #5488, #3220 ) ) ;
#13431=CARTESIAN_POINT ( 'NONE',  ( -18.05918829504999934, 10.97290950744599947, 14.00000000000000000 ) ) ;
#13437=VERTEX_POINT ( 'NONE', #9229 ) ;
#13492=FACE_OUTER_BOUND ( 'NONE', #3051, .T. ) ;
#13502=AXIS2_PLACEMENT_3D ( 'NONE', #1148, #2222, #6388 ) ;
#13526=DIRECTION ( 'NONE',  ( 1.000000000000000000, 0.000000000000000000, 0.000000000000000000 ) ) ;
#13527=PRODUCT_DEFINITION_CONTEXT ( 'detailed design', #3782, 'design' ) ;
#13531=AXIS2_PLACEMENT_3D ( 'NONE', #5161, #8437, #2958 ) ;
#13562=DIRECTION ( 'NONE',  ( -0.000000000000000000, -0.000000000000000000, 1.000000000000000000 ) ) ;
#13571=AXIS2_PLACEMENT_3D ( 'NONE', #5342, #4319, #7483 ) ;
#13578=DIRECTION ( 'NONE',  ( 1.000000000000000000, 0.000000000000000000, 0.000000000000000000 ) ) ;
#13604=AXIS2_PLACEMENT_3D ( 'NONE', #9818, #4505, #8760 ) ;
#13612=EDGE_CURVE ( 'NONE', #1587, #2494, #417, .T. ) ;
#13623=AXIS2_PLACEMENT_3D ( 'NONE', #12444, #1904, #11532 ) ;
#13663=CARTESIAN_POINT ( 'NONE',  ( -43.05918829505002066, 32.97290950744599769, 10.00000000000000000 ) ) ;
#13666=DIRECTION ( 'NONE',  ( 1.000000000000000000, 0.000000000000000000, 0.000000000000000000 ) ) ;
#13703=EDGE_LOOP ( 'NONE', ( #778, #10492, #12347, #4851 ) ) ;
#13729=FACE_BOUND ( 'NONE', #8716, .T. ) ;
#13755=CARTESIAN_POINT ( 'NONE',  ( -18.05918829504999934, 10.97290950744599947, 11.50000000000000000 ) ) ;
#13765=VERTEX_POINT ( 'NONE', #9278 ) ;
#13769=VERTEX_POINT ( 'NONE', #3079 ) ;
#13778=CARTESIAN_POINT ( 'NONE',  ( -1.059188295049996231, 27.97290950744599769, 10.00000000000000000 ) ) ;
#13785=DIRECTION ( 'NONE',  ( 0.000000000000000000, 0.000000000000000000, 1.000000000000000000 ) ) ;
#13790=ORIENTED_EDGE ( 'NONE', *, *, #1038, .T. ) ;
#13801=EDGE_CURVE ( 'NONE', #7947, #12260, #5977, .T. ) ;
ENDSEC;
END-ISO-10303-21;
